ISO-10303-21;
HEADER;
FILE_DESCRIPTION (('STEP AP214'),
    '1' );
FILE_NAME ('Screw 3.step',
    '2026-10-26T17:37:43',
    ( '' ),
    ( '' ),
    'SwSTEP 2.0',
    'SolidWorks 2024',
    '' );
FILE_SCHEMA (( 'AUTOMOTIVE_DESIGN' ));
ENDSEC;

DATA;
#83=DIRECTION ( 'NONE',  ( -5.461016542361937364E-28, 1.000000000000000000, -2.336881798971000105E-14 ) ) ;
#126=CARTESIAN_POINT ( 'NONE',  ( 12.69999999994000106, -3596.805100000000039, 2292.781800000000203 ) ) ;
#210=CARTESIAN_POINT ( 'NONE',  ( 12.69999999999999929, -3599.497499999999945, 2264.841800000000148 ) ) ;
#236=EDGE_LOOP ( 'NONE', ( #22169, #11016, #6043, #4841 ) ) ;
#302=DIRECTION ( 'NONE',  ( 2.336881798971000105E-14, 0.000000000000000000, 1.000000000000000000 ) ) ;
#348=DIRECTION ( 'NONE',  ( 0.000000000000000000, 0.000000000000000000, 1.000000000000000000 ) ) ;
#387=ORIENTED_EDGE ( 'NONE', *, *, #4635, .F. ) ;
#417=DIRECTION ( 'NONE',  ( 0.000000000000000000, 0.000000000000000000, -1.000000000000000000 ) ) ;
#431=DIRECTION ( 'NONE',  ( 1.985099921814000023E-12, 1.000000000000000000, 3.793660610075000646E-12 ) ) ;
#439=DIRECTION ( 'NONE',  ( 0.000000000000000000, 0.000000000000000000, -1.000000000000000000 ) ) ;
#455=EDGE_LOOP ( 'NONE', ( #21081, #11505 ) ) ;
#523=VERTEX_POINT ( 'NONE', #18112 ) ;
#540=DIRECTION ( 'NONE',  ( 0.8660254037824132167, -0.5000000000035080827, -5.278136500991081487E-12 ) ) ;
#556=AXIS2_PLACEMENT_3D ( 'NONE', #2349, #4217, #11140 ) ;
#562=ORIENTED_EDGE ( 'NONE', *, *, #9428, .T. ) ;
#567=CARTESIAN_POINT ( 'NONE',  ( 11.34365660141000021, -3597.148244321000220, 2296.210799999999836 ) ) ;
#568=ORIENTED_EDGE ( 'NONE', *, *, #1578, .T. ) ;
#577=EDGE_CURVE ( 'NONE', #10134, #2356, #17622, .T. ) ;
#585=EDGE_LOOP ( 'NONE', ( #11944, #15585, #11993, #17143 ) ) ;
#588=CARTESIAN_POINT ( 'NONE',  ( 10.36831320290272984, -3598.151299999887669, 2296.210799999999836 ) ) ;
#652=DIRECTION ( 'NONE',  ( -1.000000000000000000, 0.000000000000000000, 0.000000000000000000 ) ) ;
#677=ORIENTED_EDGE ( 'NONE', *, *, #19546, .F. ) ;
#782=CARTESIAN_POINT ( 'NONE',  ( 15.03168679706394428, -3598.151299999898129, 2296.210799999999836 ) ) ;
#798=DIRECTION ( 'NONE',  ( -5.682243826821398966E-14, -1.000000000000000000, 0.000000000000000000 ) ) ;
#811=AXIS2_PLACEMENT_3D ( 'NONE', #210, #439, #20016 ) ;
#904=CARTESIAN_POINT ( 'NONE',  ( 12.69999999999999929, -3596.322499999999764, 2264.841800000000148 ) ) ;
#918=EDGE_CURVE ( 'NONE', #2972, #13491, #12004, .T. ) ;
#937=( BOUNDED_CURVE ( )  B_SPLINE_CURVE ( 3, ( #23010, #5105, #1456, #12360 ),
 .UNSPECIFIED., .F., .T. ) 
 B_SPLINE_CURVE_WITH_KNOTS ( ( 4, 4 ),
 ( 1.570796327144186710, 3.141592653589829975 ),
 .UNSPECIFIED. ) 
 CURVE ( )  GEOMETRIC_REPRESENTATION_ITEM ( )  RATIONAL_B_SPLINE_CURVE ( ( 1.000000000000000000, 0.8047378542066848661, 0.8047378542066848661, 1.000000000000000000 ) ) 
 REPRESENTATION_ITEM ( '' )  );
#994=EDGE_LOOP ( 'NONE', ( #22383, #1983, #12504, #7454 ) ) ;
#1025=DIRECTION ( 'NONE',  ( 0.000000000000000000, 0.000000000000000000, 1.000000000000000000 ) ) ;
#1046=LINE ( 'NONE', #6112, #6079 ) ;
#1101=CARTESIAN_POINT ( 'NONE',  ( 15.03168679714000078, -3600.843699999999899, 2292.781800000000203 ) ) ;
#1103=DIRECTION ( 'NONE',  ( 0.8660254037840939834, -0.5000000000005969669, 0.000000000000000000 ) ) ;
#1104=CARTESIAN_POINT ( 'NONE',  ( 15.03168679714165634, -3598.151299999852654, 2296.433984632644751 ) ) ;
#1129=DIRECTION ( 'NONE',  ( 0.000000000000000000, 0.000000000000000000, 1.000000000000000000 ) ) ;
#1135=CARTESIAN_POINT ( 'NONE',  ( 10.36831320289432057, -3600.843700000111312, 2296.210799999999836 ) ) ;
#1142=CYLINDRICAL_SURFACE ( 'NONE', #15235, 5.460999999999938126 ) ;
#1150=VERTEX_POINT ( 'NONE', #6255 ) ;
#1166=DIRECTION ( 'NONE',  ( 0.8660254037816507156, 0.5000000000048288040, 0.000000000000000000 ) ) ;
#1233=TOROIDAL_SURFACE ( 'NONE', #14719, 5.080000000000000071, 0.3810000000000000053 ) ;
#1292=EDGE_LOOP ( 'NONE', ( #10333, #22643, #21659, #2923 ) ) ;
#1340=FACE_OUTER_BOUND ( 'NONE', #585, .T. ) ;
#1416=EDGE_CURVE ( 'NONE', #3958, #10503, #14554, .T. ) ;
#1456=CARTESIAN_POINT ( 'NONE',  ( 12.69999999997359375, -3596.805099999839967, 2296.433984632673855 ) ) ;
#1457=EDGE_LOOP ( 'NONE', ( #21375, #6328, #13763, #10041 ) ) ;
#1495=CARTESIAN_POINT ( 'NONE',  ( 12.69999999999999929, -3599.497499999999945, 2290.622800000000097 ) ) ;
#1515=CARTESIAN_POINT ( 'NONE',  ( 7.619999999999999218, -3599.497499999999945, 2290.241799999999785 ) ) ;
#1524=ADVANCED_FACE ( 'NONE', ( #7860 ), #18632, .F. ) ;
#1547=ADVANCED_FACE ( 'NONE', ( #2687, #15240 ), #20170, .F. ) ;
#1577=ORIENTED_EDGE ( 'NONE', *, *, #14313, .T. ) ;
#1578=EDGE_CURVE ( 'NONE', #22298, #2067, #1046, .T. ) ;
#1582=CIRCLE ( 'NONE', #17670, 3.175000000000149925 ) ;
#1623=ORIENTED_EDGE ( 'NONE', *, *, #19115, .T. ) ;
#1650=VERTEX_POINT ( 'NONE', #17447 ) ;
#1713=DIRECTION ( 'NONE',  ( -1.000000000000000000, 0.000000000000000000, -2.902585187577999742E-13 ) ) ;
#1839=FACE_OUTER_BOUND ( 'NONE', #21727, .T. ) ;
#1858=ADVANCED_FACE ( 'NONE', ( #8061 ), #4196, .T. ) ;
#1875=DIRECTION ( 'NONE',  ( -0.8660254037820785955, -0.5000000000040877302, 3.192239903039919200E-14 ) ) ;
#1909=ORIENTED_EDGE ( 'NONE', *, *, #918, .T. ) ;
#1943=DIRECTION ( 'NONE',  ( 0.000000000000000000, 0.000000000000000000, 1.000000000000000000 ) ) ;
#1968=LINE ( 'NONE', #15683, #2618 ) ;
#1975=ORIENTED_EDGE ( 'NONE', *, *, #14228, .T. ) ;
#1983=ORIENTED_EDGE ( 'NONE', *, *, #16023, .F. ) ;
#2007=EDGE_CURVE ( 'NONE', #13971, #19453, #4084, .T. ) ;
#2064=PLANE ( 'NONE',  #11030 ) ;
#2067=VERTEX_POINT ( 'NONE', #6774 ) ;
#2097=AXIS2_PLACEMENT_3D ( 'NONE', #17228, #13486, #2943 ) ;
#2117=DIRECTION ( 'NONE',  ( 0.5000000000043351989, -0.8660254037819355988, 0.000000000000000000 ) ) ;
#2144=DIRECTION ( 'NONE',  ( 0.000000000000000000, 0.000000000000000000, -1.000000000000000000 ) ) ;
#2150=EDGE_CURVE ( 'NONE', #1650, #5650, #1582, .T. ) ;
#2156=ORIENTED_EDGE ( 'NONE', *, *, #14228, .F. ) ;
#2182=PLANE ( 'NONE',  #12920 ) ;
#2184=FACE_OUTER_BOUND ( 'NONE', #10767, .T. ) ;
#2192=AXIS2_PLACEMENT_3D ( 'NONE', #15742, #5312, #10225 ) ;
#2218=DIRECTION ( 'NONE',  ( 0.8660254037816071948, 0.5000000000049040771, 0.000000000000000000 ) ) ;
#2252=ADVANCED_FACE ( 'NONE', ( #1839 ), #8985, .T. ) ;
#2257=( GEOMETRIC_REPRESENTATION_CONTEXT ( 3 ) GLOBAL_UNCERTAINTY_ASSIGNED_CONTEXT ( ( #16741 ) ) GLOBAL_UNIT_ASSIGNED_CONTEXT ( ( #21126, #3419, #23094 ) ) REPRESENTATION_CONTEXT ( 'NONE', 'WORKASPACE' ) );
#2291=CARTESIAN_POINT ( 'NONE',  ( 12.69999999994000106, -3596.805100000000039, 2292.781800000000203 ) ) ;
#2293=DIRECTION ( 'NONE',  ( 0.000000000000000000, 2.336881798971000105E-14, 1.000000000000000000 ) ) ;
#2324=VECTOR ( 'NONE', #3075, 1000.000000000000000 ) ;
#2327=ORIENTED_EDGE ( 'NONE', *, *, #20166, .T. ) ;
#2349=CARTESIAN_POINT ( 'NONE',  ( 12.69999999999999929, -3599.497499999999945, 2290.241799999999785 ) ) ;
#2356=VERTEX_POINT ( 'NONE', #11426 ) ;
#2357=DIRECTION ( 'NONE',  ( 1.000000000000000000, 0.000000000000000000, 0.000000000000000000 ) ) ;
#2361=VECTOR ( 'NONE', #540, 1000.000000000000227 ) ;
#2362=CARTESIAN_POINT ( 'NONE',  ( 10.36831320283000046, -3600.843699999999899, 2296.210799999999836 ) ) ;
#2383=EDGE_CURVE ( 'NONE', #13491, #6446, #6849, .T. ) ;
#2384=CARTESIAN_POINT ( 'NONE',  ( 15.18950216443630374, -3600.934814744946834, 2296.591800000036528 ) ) ;
#2391=CARTESIAN_POINT ( 'NONE',  ( 15.03168679714000078, -3600.843699999999899, 2292.781800000000203 ) ) ;
#2400=AXIS2_PLACEMENT_3D ( 'NONE', #1495, #18132, #16490 ) ;
#2413=DIRECTION ( 'NONE',  ( 0.000000000000000000, 0.000000000000000000, 1.000000000000000000 ) ) ;
#2414=CARTESIAN_POINT ( 'NONE',  ( 10.36831320290272984, -3598.151299999887669, 2296.210799999999836 ) ) ;
#2415=DIRECTION ( 'NONE',  ( 0.000000000000000000, -1.000000000000000000, 0.000000000000000000 ) ) ;
#2430=EDGE_CURVE ( 'NONE', #7722, #13032, #9449, .T. ) ;
#2436=VECTOR ( 'NONE', #14637, 1000.000000000000000 ) ;
#2474=CARTESIAN_POINT ( 'NONE',  ( 12.69999999999999929, -3599.497499999999945, 2290.241799999999785 ) ) ;
#2528=DIRECTION ( 'NONE',  ( -1.000000000000000000, 1.206520773835000154E-12, 0.000000000000000000 ) ) ;
#2544=ORIENTED_EDGE ( 'NONE', *, *, #3855, .T. ) ;
#2569=DIRECTION ( 'NONE',  ( 0.000000000000000000, 0.000000000000000000, 1.000000000000000000 ) ) ;
#2606=CARTESIAN_POINT ( 'NONE',  ( 0.000000000000000000, 0.000000000000000000, 0.000000000000000000 ) ) ;
#2607=FACE_OUTER_BOUND ( 'NONE', #17094, .T. ) ;
#2618=VECTOR ( 'NONE', #5728, 1000.000000000000000 ) ;
#2648=CARTESIAN_POINT ( 'NONE',  ( 12.69999999999999929, -3599.497499999999945, 2264.841800000000148 ) ) ;
#2658=DIRECTION ( 'NONE',  ( -0.5000000000048030468, 0.8660254037816655925, 0.000000000000000000 ) ) ;
#2675=VECTOR ( 'NONE', #3797, 1000.000000000000000 ) ;
#2687=FACE_BOUND ( 'NONE', #455, .T. ) ;
#2760=EDGE_CURVE ( 'NONE', #3526, #7722, #18406, .T. ) ;
#2888=VERTEX_POINT ( 'NONE', #15125 ) ;
#2899=CARTESIAN_POINT ( 'NONE',  ( 12.69999999999999929, -3599.497499999999945, 2290.241799999999785 ) ) ;
#2905=EDGE_LOOP ( 'NONE', ( #20352, #4001, #21345, #6760 ) ) ;
#2923=ORIENTED_EDGE ( 'NONE', *, *, #13534, .T. ) ;
#2943=DIRECTION ( 'NONE',  ( 0.000000000000000000, -1.000000000000000000, 0.000000000000000000 ) ) ;
#2944=DIRECTION ( 'NONE',  ( -2.848812946084999742E-12, -1.000000000000000000, 0.000000000000000000 ) ) ;
#2972=VERTEX_POINT ( 'NONE', #4919 ) ;
#2987=EDGE_CURVE ( 'NONE', #13032, #6140, #19100, .T. ) ;
#3013=ORIENTED_EDGE ( 'NONE', *, *, #16965, .F. ) ;
#3075=DIRECTION ( 'NONE',  ( 1.105405881099000035E-12, 1.000000000000000000, 0.000000000000000000 ) ) ;
#3097=CARTESIAN_POINT ( 'NONE',  ( 14.05634339854999837, -3597.148244321000220, 2296.210799999999836 ) ) ;
#3125=DIRECTION ( 'NONE',  ( -5.682243826821398966E-14, -1.000000000000000000, 0.000000000000000000 ) ) ;
#3161=CIRCLE ( 'NONE', #16272, 1.269999999999882334 ) ;
#3254=EDGE_CURVE ( 'NONE', #6140, #14734, #21757, .T. ) ;
#3270=VECTOR ( 'NONE', #7761, 1000.000000000000000 ) ;
#3282=VECTOR ( 'NONE', #12975, 1000.000000000000000 ) ;
#3355=DIRECTION ( 'NONE',  ( 0.5000000000031962211, 0.8660254037825932949, 0.000000000000000000 ) ) ;
#3369=FACE_BOUND ( 'NONE', #4155, .T. ) ;
#3384=ORIENTED_EDGE ( 'NONE', *, *, #13984, .F. ) ;
#3388=PRODUCT_DEFINITION_SHAPE ( 'NONE', 'NONE',  #3469 ) ;
#3400=CARTESIAN_POINT ( 'NONE',  ( 14.05634339857000015, -3601.846755679000125, 2296.210799999999836 ) ) ;
#3419=( NAMED_UNIT ( * ) PLANE_ANGLE_UNIT ( ) SI_UNIT ( $, .RADIAN. ) );
#3436=AXIS2_PLACEMENT_3D ( 'NONE', #22401, #21132, #10341 ) ;
#3449=DIRECTION ( 'NONE',  ( 0.000000000000000000, 0.000000000000000000, -1.000000000000000000 ) ) ;
#3469=PRODUCT_DEFINITION ( 'UNKNOWN', '', #16085, #8320 ) ;
#3526=VERTEX_POINT ( 'NONE', #19874 ) ;
#3535=CARTESIAN_POINT ( 'NONE',  ( 12.69999999999999929, -3601.402499999999691, 2263.571799999999712 ) ) ;
#3609=EDGE_CURVE ( 'NONE', #10134, #22010, #18608, .T. ) ;
#3639=VERTEX_POINT ( 'NONE', #3535 ) ;
#3660=ADVANCED_FACE ( 'NONE', ( #19602 ), #21362, .T. ) ;
#3693=DIRECTION ( 'NONE',  ( 0.000000000000000000, -2.336881798971000105E-14, -1.000000000000000000 ) ) ;
#3698=ORIENTED_EDGE ( 'NONE', *, *, #2383, .T. ) ;
#3702=ADVANCED_FACE ( 'NONE', ( #14214 ), #11038, .T. ) ;
#3766=DIRECTION ( 'NONE',  ( 0.000000000000000000, 0.000000000000000000, -1.000000000000000000 ) ) ;
#3784=EDGE_CURVE ( 'NONE', #8549, #13491, #20295, .T. ) ;
#3797=DIRECTION ( 'NONE',  ( -0.8660254037826616846, 0.5000000000030777603, 0.000000000000000000 ) ) ;
#3808=CARTESIAN_POINT ( 'NONE',  ( 15.03168679714000078, -3600.843699999999899, 2292.781800000000203 ) ) ;
#3854=ORIENTED_EDGE ( 'NONE', *, *, #1578, .F. ) ;
#3855=EDGE_CURVE ( 'NONE', #3639, #2356, #6278, .T. ) ;
#3902=TOROIDAL_SURFACE ( 'NONE', #2400, 5.080000000000000071, 0.3810000000000000053 ) ;
#3958=VERTEX_POINT ( 'NONE', #21102 ) ;
#4001=ORIENTED_EDGE ( 'NONE', *, *, #16023, .T. ) ;
#4019=ORIENTED_EDGE ( 'NONE', *, *, #4790, .F. ) ;
#4026=ORIENTED_EDGE ( 'NONE', *, *, #8090, .F. ) ;
#4065=EDGE_CURVE ( 'NONE', #1150, #3958, #10315, .T. ) ;
#4071=ORIENTED_EDGE ( 'NONE', *, *, #14140, .F. ) ;
#4079=EDGE_CURVE ( 'NONE', #3526, #13971, #17459, .T. ) ;
#4084=LINE ( 'NONE', #18708, #21796 ) ;
#4155=EDGE_LOOP ( 'NONE', ( #11359, #6341, #10311, #11892, #9276, #21554 ) ) ;
#4157=CARTESIAN_POINT ( 'NONE',  ( 12.69999999999999929, -3599.497499999999945, 2290.622800000000097 ) ) ;
#4159=CARTESIAN_POINT ( 'NONE',  ( 12.69999999999999929, -3604.958499999999731, 2290.622800000000097 ) ) ;
#4196=CYLINDRICAL_SURFACE ( 'NONE', #5721, 0.3809999999999303388 ) ;
#4210=VECTOR ( 'NONE', #17659, 1000.000000000000000 ) ;
#4217=DIRECTION ( 'NONE',  ( 0.000000000000000000, -2.336881798971000105E-14, -1.000000000000000000 ) ) ;
#4234=ORIENTED_EDGE ( 'NONE', *, *, #4079, .T. ) ;
#4288=AXIS2_PLACEMENT_3D ( 'NONE', #2648, #22436, #7933 ) ;
#4297=CARTESIAN_POINT ( 'NONE',  ( 17.78000000000000114, -3599.497499999999945, 2290.622800000000097 ) ) ;
#4394=VECTOR ( 'NONE', #1166, 1000.000000000000114 ) ;
#4439=FACE_OUTER_BOUND ( 'NONE', #20191, .T. ) ;
#4448=ORIENTED_EDGE ( 'NONE', *, *, #10833, .T. ) ;
#4467=VERTEX_POINT ( 'NONE', #20955 ) ;
#4562=DIRECTION ( 'NONE',  ( 2.336881798971000105E-14, 2.336881798971000105E-14, 1.000000000000000000 ) ) ;
#4595=DIRECTION ( 'NONE',  ( 2.848812946084999742E-12, 1.000000000000000000, -2.336881798978000141E-14 ) ) ;
#4635=EDGE_CURVE ( 'NONE', #2888, #17496, #1968, .T. ) ;
#4648=FACE_OUTER_BOUND ( 'NONE', #15083, .T. ) ;
#4663=CARTESIAN_POINT ( 'NONE',  ( 12.69999999999999929, -3599.497499999999945, 2290.241799999999785 ) ) ;
#4765=DIRECTION ( 'NONE',  ( -1.000000000000000000, 5.461016542361937364E-28, 2.336881798970999789E-14 ) ) ;
#4790=EDGE_CURVE ( 'NONE', #4467, #19050, #4881, .T. ) ;
#4841=ORIENTED_EDGE ( 'NONE', *, *, #8064, .F. ) ;
#4881=CIRCLE ( 'NONE', #10877, 0.3809999999999647002 ) ;
#4890=CARTESIAN_POINT ( 'NONE',  ( 7.238999999999998991, -3599.497499999999945, 2290.622800000000552 ) ) ;
#4892=ADVANCED_BREP_SHAPE_REPRESENTATION ( '', ( #13798, #5611 ), #16462 ) ;
#4919=CARTESIAN_POINT ( 'NONE',  ( 18.16100000000000136, -3599.497499999999945, 2296.210799999999836 ) ) ;
#4925=CARTESIAN_POINT ( 'NONE',  ( 9.987313202835000681, -3597.931329546999677, 2296.591799999999694 ) ) ;
#4927=AXIS2_PLACEMENT_3D ( 'NONE', #19255, #17360, #15500 ) ;
#4934=LINE ( 'NONE', #2291, #5058 ) ;
#4978=CARTESIAN_POINT ( 'NONE',  ( 12.69999999996000106, -3602.189899999999852, 2296.210799999999836 ) ) ;
#5058=VECTOR ( 'NONE', #9437, 1000.000000000000000 ) ;
#5078=VECTOR ( 'NONE', #15724, 1000.000000000000000 ) ;
#5104=DIRECTION ( 'NONE',  ( -0.8660254037824819395, 0.5000000000033889558, 0.000000000000000000 ) ) ;
#5105=CARTESIAN_POINT ( 'NONE',  ( 12.69999999997316742, -3596.622870510377652, 2296.591799999921477 ) ) ;
#5155=EDGE_LOOP ( 'NONE', ( #14576, #1623 ) ) ;
#5172=DIRECTION ( 'NONE',  ( 2.803365712371000161E-12, 1.000000000000000000, 0.000000000000000000 ) ) ;
#5269=EDGE_LOOP ( 'NONE', ( #568, #13962, #11749, #12698 ) ) ;
#5298=DIRECTION ( 'NONE',  ( 0.8660254037840259267, -0.5000000000007149836, 0.000000000000000000 ) ) ;
#5312=DIRECTION ( 'NONE',  ( -0.8660254037825932949, 0.5000000000031962211, 0.000000000000000000 ) ) ;
#5331=LINE ( 'NONE', #4978, #15821 ) ;
#5353=ORIENTED_EDGE ( 'NONE', *, *, #2987, .F. ) ;
#5472=CARTESIAN_POINT ( 'NONE',  ( 7.619999999999999218, -3599.497499999999945, 2296.591799999999694 ) ) ;
#5480=( BOUNDED_CURVE ( )  B_SPLINE_CURVE ( 3, ( #17187, #13806, #8296, #1135 ),
 .UNSPECIFIED., .F., .T. ) 
 B_SPLINE_CURVE_WITH_KNOTS ( ( 4, 4 ),
 ( 1.570796327106734891, 3.141592653589766471 ),
 .UNSPECIFIED. ) 
 CURVE ( )  GEOMETRIC_REPRESENTATION_ITEM ( )  RATIONAL_B_SPLINE_CURVE ( ( 1.000000000000000000, 0.8047378541978723598, 0.8047378541978723598, 1.000000000000000000 ) ) 
 REPRESENTATION_ITEM ( '' )  );
#5487=DIRECTION ( 'NONE',  ( -0.5000000000005969669, -0.8660254037840939834, 0.000000000000000000 ) ) ;
#5503=FACE_OUTER_BOUND ( 'NONE', #16844, .T. ) ;
#5520=VECTOR ( 'NONE', #16073, 1000.000000000000000 ) ;
#5529=ADVANCED_FACE ( 'NONE', ( #21451 ), #19458, .T. ) ;
#5548=SHAPE_REPRESENTATION_RELATIONSHIP ( 'NONE' , 'NONE' ,  #18056, #4892 ) ;
#5601=DIRECTION ( 'NONE',  ( -0.8660254037840939834, 0.5000000000005969669, 0.000000000000000000 ) ) ;
#5611=AXIS2_PLACEMENT_3D ( 'NONE', #2606, #9751, #7545 ) ;
#5650=VERTEX_POINT ( 'NONE', #21908 ) ;
#5700=DIRECTION ( 'NONE',  ( 0.000000000000000000, 0.000000000000000000, 1.000000000000000000 ) ) ;
#5714=CARTESIAN_POINT ( 'NONE',  ( 10.36831320283000046, -3600.843699999999899, 2292.781800000000203 ) ) ;
#5716=ADVANCED_FACE ( 'NONE', ( #4439 ), #1142, .T. ) ;
#5721=AXIS2_PLACEMENT_3D ( 'NONE', #567, #14873, #2658 ) ;
#5728=DIRECTION ( 'NONE',  ( -0.8660254037843172492, 0.5000000000002102762, 3.628718844336076700E-12 ) ) ;
#5847=VECTOR ( 'NONE', #21321, 1000.000000000000000 ) ;
#5880=CARTESIAN_POINT ( 'NONE',  ( 12.69999999997359019, -3596.805099999930007, 2296.210799999999836 ) ) ;
#5964=CARTESIAN_POINT ( 'NONE',  ( 15.41268679713999923, -3601.063670452999759, 2296.591799999999694 ) ) ;
#6000=ORIENTED_EDGE ( 'NONE', *, *, #20824, .F. ) ;
#6043=ORIENTED_EDGE ( 'NONE', *, *, #2007, .T. ) ;
#6079=VECTOR ( 'NONE', #8202, 1000.000000000000000 ) ;
#6112=CARTESIAN_POINT ( 'NONE',  ( 15.03168679714000078, -3598.151299999999992, 2296.210799999999836 ) ) ;
#6140=VERTEX_POINT ( 'NONE', #18696 ) ;
#6151=LINE ( 'NONE', #15055, #11108 ) ;
#6185=AXIS2_PLACEMENT_3D ( 'NONE', #4157, #6708, #13172 ) ;
#6255=CARTESIAN_POINT ( 'NONE',  ( 9.987313202835000681, -3597.931329547144287, 2296.591799999999694 ) ) ;
#6260=CARTESIAN_POINT ( 'NONE',  ( 9.987313202833000503, -3599.497499999999945, 2296.210799999999836 ) ) ;
#6278=CIRCLE ( 'NONE', #19001, 1.904999999999823501 ) ;
#6287=LINE ( 'NONE', #1101, #6474 ) ;
#6319=ORIENTED_EDGE ( 'NONE', *, *, #11634, .T. ) ;
#6328=ORIENTED_EDGE ( 'NONE', *, *, #14021, .F. ) ;
#6341=ORIENTED_EDGE ( 'NONE', *, *, #4065, .T. ) ;
#6367=ORIENTED_EDGE ( 'NONE', *, *, #19271, .T. ) ;
#6395=DIRECTION ( 'NONE',  ( -0.8660254037817188832, -0.5000000000047110094, 1.319534125263029996E-12 ) ) ;
#6446=VERTEX_POINT ( 'NONE', #11409 ) ;
#6470=CYLINDRICAL_SURFACE ( 'NONE', #2097, 3.175000000000149925 ) ;
#6474=VECTOR ( 'NONE', #13302, 1000.000000000000000 ) ;
#6476=APPLICATION_CONTEXT ( 'configuration controlled 3d designs of mechanical parts and assemblies' ) ;
#6553=PLANE ( 'NONE',  #19686 ) ;
#6554=AXIS2_PLACEMENT_3D ( 'NONE', #12585, #19614, #12696 ) ;
#6573=ORIENTED_EDGE ( 'NONE', *, *, #19115, .F. ) ;
#6579=EDGE_CURVE ( 'NONE', #13032, #23163, #6151, .T. ) ;
#6708=DIRECTION ( 'NONE',  ( 2.336881798971000105E-14, 2.336881798971000105E-14, 1.000000000000000000 ) ) ;
#6712=LINE ( 'NONE', #8579, #5078 ) ;
#6715=LINE ( 'NONE', #22974, #15923 ) ;
#6727=FACE_OUTER_BOUND ( 'NONE', #14311, .T. ) ;
#6760=ORIENTED_EDGE ( 'NONE', *, *, #3855, .F. ) ;
#6774=CARTESIAN_POINT ( 'NONE',  ( 15.03168679707234467, -3600.843700000039007, 2296.210799999999836 ) ) ;
#6840=ADVANCED_FACE ( 'NONE', ( #18647 ), #6470, .T. ) ;
#6849=CIRCLE ( 'NONE', #21079, 5.460999999999938126 ) ;
#6870=ORIENTED_EDGE ( 'NONE', *, *, #15737, .F. ) ;
#6924=AXIS2_PLACEMENT_3D ( 'NONE', #20543, #2293, #11303 ) ;
#6957=CYLINDRICAL_SURFACE ( 'NONE', #2192, 0.3810000000000260956 ) ;
#6959=PRODUCT ( 'Screw 3', 'Screw 3', '', ( #16676 ) ) ;
#6967=ORIENTED_EDGE ( 'NONE', *, *, #21178, .F. ) ;
#7205=LINE ( 'NONE', #9425, #12085 ) ;
#7367=ORIENTED_EDGE ( 'NONE', *, *, #13534, .F. ) ;
#7390=DIRECTION ( 'NONE',  ( -1.000000000000000000, 5.461016542361937364E-28, 2.336881798970999789E-14 ) ) ;
#7430=ORIENTED_EDGE ( 'NONE', *, *, #4635, .T. ) ;
#7450=CARTESIAN_POINT ( 'NONE',  ( 18.16100000000000136, -3599.497499999999945, 2290.622800000000097 ) ) ;
#7454=ORIENTED_EDGE ( 'NONE', *, *, #10999, .F. ) ;
#7463=CARTESIAN_POINT ( 'NONE',  ( 10.36831320283000046, -3600.843699999999899, 2292.781800000000203 ) ) ;
#7479=VERTEX_POINT ( 'NONE', #10335 ) ;
#7545=DIRECTION ( 'NONE',  ( 1.000000000000000000, 0.000000000000000000, 0.000000000000000000 ) ) ;
#7588=CIRCLE ( 'NONE', #9818, 5.460999999999938126 ) ;
#7592=ORIENTED_EDGE ( 'NONE', *, *, #2430, .T. ) ;
#7627=DIRECTION ( 'NONE',  ( -5.461016542361937364E-28, 1.000000000000000000, -2.336881798971000105E-14 ) ) ;
#7679=CIRCLE ( 'NONE', #10673, 5.460999999999938126 ) ;
#7682=DIRECTION ( 'NONE',  ( 2.336881798971000105E-14, 0.000000000000000000, 1.000000000000000000 ) ) ;
#7687=DIRECTION ( 'NONE',  ( 2.336881798971000105E-14, 0.000000000000000000, 1.000000000000000000 ) ) ;
#7696=CIRCLE ( 'NONE', #8460, 5.460999999999938126 ) ;
#7722=VERTEX_POINT ( 'NONE', #23149 ) ;
#7756=ORIENTED_EDGE ( 'NONE', *, *, #2760, .F. ) ;
#7761=DIRECTION ( 'NONE',  ( 0.000000000000000000, 0.000000000000000000, 1.000000000000000000 ) ) ;
#7767=ORIENTED_EDGE ( 'NONE', *, *, #20824, .T. ) ;
#7773=CARTESIAN_POINT ( 'NONE',  ( 15.03168679713838074, -3600.843700000154968, 2296.433984632765259 ) ) ;
#7801=DIRECTION ( 'NONE',  ( 0.000000000000000000, 0.000000000000000000, 1.000000000000000000 ) ) ;
#7831=EDGE_LOOP ( 'NONE', ( #18424, #7367, #4071, #6367 ) ) ;
#7851=CARTESIAN_POINT ( 'NONE',  ( 10.21049783553828050, -3598.060185255057604, 2296.591800000037438 ) ) ;
#7860=FACE_OUTER_BOUND ( 'NONE', #20161, .T. ) ;
#7864=EDGE_CURVE ( 'NONE', #7722, #7479, #9452, .T. ) ;
#7933=DIRECTION ( 'NONE',  ( 0.000000000000000000, 1.000000000000000000, 0.000000000000000000 ) ) ;
#7936=CARTESIAN_POINT ( 'NONE',  ( 12.69999999999143903, -3602.372129489641338, 2296.591799999931936 ) ) ;
#7966=ORIENTED_EDGE ( 'NONE', *, *, #19119, .F. ) ;
#7998=EDGE_CURVE ( 'NONE', #22298, #10503, #19360, .T. ) ;
#8053=CARTESIAN_POINT ( 'NONE',  ( 12.69999999999999929, -3599.497499999999945, 2290.622800000000097 ) ) ;
#8061=FACE_OUTER_BOUND ( 'NONE', #236, .T. ) ;
#8064=EDGE_CURVE ( 'NONE', #3958, #19453, #937, .T. ) ;
#8090=EDGE_CURVE ( 'NONE', #2972, #9357, #8721, .T. ) ;
#8127=DIRECTION ( 'NONE',  ( 0.000000000000000000, -1.000000000000000000, 0.000000000000000000 ) ) ;
#8168=CARTESIAN_POINT ( 'NONE',  ( 12.69999999997562057, -3602.189900000083526, 2296.210799999999836 ) ) ;
#8202=DIRECTION ( 'NONE',  ( -1.286674632898999957E-12, -1.000000000000000000, 0.000000000000000000 ) ) ;
#8291=ORIENTED_EDGE ( 'NONE', *, *, #3254, .T. ) ;
#8296=CARTESIAN_POINT ( 'NONE',  ( 10.36831320282916380, -3600.843700000149056, 2296.433984632680676 ) ) ;
#8320=PRODUCT_DEFINITION_CONTEXT ( 'detailed design', #6476, 'design' ) ;
#8362=FACE_OUTER_BOUND ( 'NONE', #994, .T. ) ;
#8460=AXIS2_PLACEMENT_3D ( 'NONE', #8053, #17177, #15317 ) ;
#8504=CYLINDRICAL_SURFACE ( 'NONE', #11721, 0.3809999999999154618 ) ;
#8549=VERTEX_POINT ( 'NONE', #17247 ) ;
#8553=ORIENTED_EDGE ( 'NONE', *, *, #577, .F. ) ;
#8579=CARTESIAN_POINT ( 'NONE',  ( 15.03168679714000078, -3598.151299999999992, 2292.781800000000203 ) ) ;
#8721=CIRCLE ( 'NONE', #21819, 0.3809999999999647002 ) ;
#8724=EDGE_LOOP ( 'NONE', ( #19033, #8291, #16208, #21003 ) ) ;
#8735=AXIS2_PLACEMENT_3D ( 'NONE', #6260, #4595, #9867 ) ;
#8766=CARTESIAN_POINT ( 'NONE',  ( 17.78000000000000114, -3599.497499999999945, 2296.591799999999694 ) ) ;
#8789=CYLINDRICAL_SURFACE ( 'NONE', #17873, 5.460999999999938126 ) ;
#8937=DIRECTION ( 'NONE',  ( -1.206520773835000154E-12, -1.000000000000000000, 2.336881798973999985E-14 ) ) ;
#8954=DIRECTION ( 'NONE',  ( 2.336881798971000105E-14, 0.000000000000000000, 1.000000000000000000 ) ) ;
#8985=PLANE ( 'NONE',  #20309 ) ;
#9001=ADVANCED_FACE ( 'NONE', ( #10891 ), #8789, .T. ) ;
#9087=CIRCLE ( 'NONE', #16206, 0.3809999999999647002 ) ;
#9118=FACE_OUTER_BOUND ( 'NONE', #2905, .T. ) ;
#9258=UNCERTAINTY_MEASURE_WITH_UNIT (LENGTH_MEASURE( 1.000000000000000082E-05 ), #17942, 'distance_accuracy_value', 'NONE');
#9276=ORIENTED_EDGE ( 'NONE', *, *, #12393, .T. ) ;
#9286=DIRECTION ( 'NONE',  ( 0.000000000000000000, 0.000000000000000000, 1.000000000000000000 ) ) ;
#9357=VERTEX_POINT ( 'NONE', #8766 ) ;
#9425=CARTESIAN_POINT ( 'NONE',  ( 12.69999999999999929, -3596.322499999999764, 2264.841800000000148 ) ) ;
#9428=EDGE_CURVE ( 'NONE', #2888, #22298, #15158, .T. ) ;
#9437=DIRECTION ( 'NONE',  ( 7.082568872520999671E-14, 3.885294924354999670E-13, 1.000000000000000000 ) ) ;
#9449=LINE ( 'NONE', #5714, #2361 ) ;
#9452=LINE ( 'NONE', #7463, #12858 ) ;
#9453=ORIENTED_EDGE ( 'NONE', *, *, #15232, .F. ) ;
#9492=CARTESIAN_POINT ( 'NONE',  ( 9.987313202835000681, -3597.931329547144287, 2296.591799999999694 ) ) ;
#9519=TOROIDAL_SURFACE ( 'NONE', #4288, 1.905000000000000027, 1.270000000000000018 ) ;
#9551=CARTESIAN_POINT ( 'NONE',  ( 12.69999999999999929, -3597.592500000000200, 2264.841800000000148 ) ) ;
#9615=ORIENTED_EDGE ( 'NONE', *, *, #3784, .T. ) ;
#9640=ORIENTED_EDGE ( 'NONE', *, *, #15830, .F. ) ;
#9649=ADVANCED_FACE ( 'NONE', ( #6727 ), #6957, .T. ) ;
#9749=ORIENTED_EDGE ( 'NONE', *, *, #16965, .T. ) ;
#9750=DIRECTION ( 'NONE',  ( 0.000000000000000000, 1.000000000000000000, 0.000000000000000000 ) ) ;
#9751=DIRECTION ( 'NONE',  ( 0.000000000000000000, 0.000000000000000000, 1.000000000000000000 ) ) ;
#9807=EDGE_LOOP ( 'NONE', ( #4026, #1909, #3698, #10191, #11367 ) ) ;
#9818=AXIS2_PLACEMENT_3D ( 'NONE', #21274, #12122, #19506 ) ;
#9867=DIRECTION ( 'NONE',  ( -1.000000000000000000, 2.331176954593508450E-12, 0.000000000000000000 ) ) ;
#9907=CIRCLE ( 'NONE', #18882, 5.080000000000000959 ) ;
#9912=ORIENTED_EDGE ( 'NONE', *, *, #21246, .F. ) ;
#9945=TOROIDAL_SURFACE ( 'NONE', #15949, 5.080000000000000071, 0.3810000000000000053 ) ;
#10036=ORIENTED_EDGE ( 'NONE', *, *, #16521, .F. ) ;
#10041=ORIENTED_EDGE ( 'NONE', *, *, #2987, .T. ) ;
#10105=CYLINDRICAL_SURFACE ( 'NONE', #4927, 3.175000000000149925 ) ;
#10134=VERTEX_POINT ( 'NONE', #904 ) ;
#10135=LINE ( 'NONE', #13539, #12021 ) ;
#10191=ORIENTED_EDGE ( 'NONE', *, *, #13984, .T. ) ;
#10213=ORIENTED_EDGE ( 'NONE', *, *, #19514, .F. ) ;
#10225=DIRECTION ( 'NONE',  ( -0.5000000000031612490, -0.8660254037826135010, 0.000000000000000000 ) ) ;
#10267=ADVANCED_FACE ( 'NONE', ( #3369, #10522 ), #6553, .T. ) ;
#10311=ORIENTED_EDGE ( 'NONE', *, *, #1416, .T. ) ;
#10315=LINE ( 'NONE', #4925, #4394 ) ;
#10333=ORIENTED_EDGE ( 'NONE', *, *, #4079, .F. ) ;
#10335=CARTESIAN_POINT ( 'NONE',  ( 10.36831320284000135, -3598.151299999999992, 2292.781800000000203 ) ) ;
#10341=DIRECTION ( 'NONE',  ( 0.000000000000000000, 1.000000000000000000, 0.000000000000000000 ) ) ;
#10441=AXIS2_PLACEMENT_3D ( 'NONE', #19419, #3355, #17065 ) ;
#10503=VERTEX_POINT ( 'NONE', #19275 ) ;
#10522=FACE_OUTER_BOUND ( 'NONE', #12100, .T. ) ;
#10673=AXIS2_PLACEMENT_3D ( 'NONE', #15956, #10793, #20251 ) ;
#10701=ORIENTED_EDGE ( 'NONE', *, *, #21630, .T. ) ;
#10767=EDGE_LOOP ( 'NONE', ( #7592, #17682, #6967, #7430, #13847, #11340 ) ) ;
#10793=DIRECTION ( 'NONE',  ( -2.336881798971000105E-14, 0.000000000000000000, -1.000000000000000000 ) ) ;
#10823=ORIENTED_EDGE ( 'NONE', *, *, #21246, .T. ) ;
#10833=EDGE_CURVE ( 'NONE', #2356, #3639, #11458, .T. ) ;
#10877=AXIS2_PLACEMENT_3D ( 'NONE', #4297, #16378, #21655 ) ;
#10891=FACE_OUTER_BOUND ( 'NONE', #22651, .T. ) ;
#10899=DIRECTION ( 'NONE',  ( 2.336881798971000105E-14, 2.336881798971000105E-14, 1.000000000000000000 ) ) ;
#10945=DIRECTION ( 'NONE',  ( 0.000000000000000000, 0.000000000000000000, 1.000000000000000000 ) ) ;
#10999=EDGE_CURVE ( 'NONE', #5650, #1650, #15934, .T. ) ;
#11016=ORIENTED_EDGE ( 'NONE', *, *, #19546, .T. ) ;
#11030=AXIS2_PLACEMENT_3D ( 'NONE', #17995, #14606, #1713 ) ;
#11038=CYLINDRICAL_SURFACE ( 'NONE', #16377, 0.3810000000000011156 ) ;
#11092=CARTESIAN_POINT ( 'NONE',  ( 12.69999999999999929, -3599.497499999999945, 2296.210799999999836 ) ) ;
#11108=VECTOR ( 'NONE', #15505, 1000.000000000000114 ) ;
#11140=DIRECTION ( 'NONE',  ( 1.000000000000000000, 0.000000000000000000, 0.000000000000000000 ) ) ;
#11160=DIRECTION ( 'NONE',  ( 0.000000000000000000, 1.000000000000000000, 0.000000000000000000 ) ) ;
#11202=CARTESIAN_POINT ( 'NONE',  ( 15.03168679714000078, -3598.151299999999992, 2292.781800000000203 ) ) ;
#11261=CARTESIAN_POINT ( 'NONE',  ( 12.70000000023333264, -3602.629840905158289, 2296.591799999999694 ) ) ;
#11303=DIRECTION ( 'NONE',  ( -1.000000000000000000, 0.000000000000000000, 0.000000000000000000 ) ) ;
#11340=ORIENTED_EDGE ( 'NONE', *, *, #7864, .F. ) ;
#11359=ORIENTED_EDGE ( 'NONE', *, *, #21349, .F. ) ;
#11367=ORIENTED_EDGE ( 'NONE', *, *, #11634, .F. ) ;
#11373=ORIENTED_EDGE ( 'NONE', *, *, #21349, .T. ) ;
#11409=CARTESIAN_POINT ( 'NONE',  ( 7.238999999999998991, -3599.497499999999945, 2296.210799999999836 ) ) ;
#11426=CARTESIAN_POINT ( 'NONE',  ( 12.69999999999999929, -3597.592500000000200, 2263.571799999999712 ) ) ;
#11458=CIRCLE ( 'NONE', #12595, 1.904999999999823501 ) ;
#11469=ORIENTED_EDGE ( 'NONE', *, *, #3609, .T. ) ;
#11481=ORIENTED_EDGE ( 'NONE', *, *, #14233, .T. ) ;
#11488=VERTEX_POINT ( 'NONE', #5472 ) ;
#11504=CARTESIAN_POINT ( 'NONE',  ( 15.03168679707234467, -3600.843700000039007, 2296.210799999999836 ) ) ;
#11505=ORIENTED_EDGE ( 'NONE', *, *, #10999, .T. ) ;
#11536=CARTESIAN_POINT ( 'NONE',  ( 12.69999999994000106, -3596.805100000000039, 2292.781800000000203 ) ) ;
#11547=ADVANCED_FACE ( 'NONE', ( #2184 ), #2064, .F. ) ;
#11580=LINE ( 'NONE', #21434, #5847 ) ;
#11590=VERTEX_POINT ( 'NONE', #4159 ) ;
#11599=CARTESIAN_POINT ( 'NONE',  ( 12.69999999999999929, -3599.497499999999945, 2263.571799999999712 ) ) ;
#11621=AXIS2_PLACEMENT_3D ( 'NONE', #14809, #8954, #13048 ) ;
#11634=EDGE_CURVE ( 'NONE', #9357, #11488, #22234, .T. ) ;
#11668=LINE ( 'NONE', #22569, #16673 ) ;
#11705=CIRCLE ( 'NONE', #12105, 5.460999999999938126 ) ;
#11721=AXIS2_PLACEMENT_3D ( 'NONE', #3097, #1103, #16077 ) ;
#11722=CARTESIAN_POINT ( 'NONE',  ( 15.41268679713999923, -3601.063670452857423, 2296.591799999999694 ) ) ;
#11749=ORIENTED_EDGE ( 'NONE', *, *, #16075, .T. ) ;
#11892=ORIENTED_EDGE ( 'NONE', *, *, #16075, .F. ) ;
#11944=ORIENTED_EDGE ( 'NONE', *, *, #16521, .T. ) ;
#11947=AXIS2_PLACEMENT_3D ( 'NONE', #11202, #2528, #2413 ) ;
#11993=ORIENTED_EDGE ( 'NONE', *, *, #1416, .F. ) ;
#11998=ORIENTED_EDGE ( 'NONE', *, *, #14233, .F. ) ;
#12004=CIRCLE ( 'NONE', #11621, 5.460999999999938126 ) ;
#12021=VECTOR ( 'NONE', #19285, 1000.000000000000000 ) ;
#12085=VECTOR ( 'NONE', #10945, 1000.000000000000000 ) ;
#12100=EDGE_LOOP ( 'NONE', ( #7767, #6319 ) ) ;
#12105=AXIS2_PLACEMENT_3D ( 'NONE', #22279, #22513, #8127 ) ;
#12122=DIRECTION ( 'NONE',  ( -2.336881798971000105E-14, 0.000000000000000000, -1.000000000000000000 ) ) ;
#12123=DIRECTION ( 'NONE',  ( -1.224646799141892071E-16, -1.000000000000000000, 2.336881798971000421E-14 ) ) ;
#12273=PLANE ( 'NONE',  #10441 ) ;
#12360=CARTESIAN_POINT ( 'NONE',  ( 12.69999999997359019, -3596.805099999930007, 2296.210799999999836 ) ) ;
#12393=EDGE_CURVE ( 'NONE', #17394, #14734, #18140, .T. ) ;
#12504=ORIENTED_EDGE ( 'NONE', *, *, #15737, .T. ) ;
#12585=CARTESIAN_POINT ( 'NONE',  ( 12.69999999999999929, -3599.497499999999945, 2296.591799999999694 ) ) ;
#12595=AXIS2_PLACEMENT_3D ( 'NONE', #13393, #14813, #9750 ) ;
#12696=DIRECTION ( 'NONE',  ( -1.000000000000000000, 0.000000000000000000, 0.000000000000000000 ) ) ;
#12698=ORIENTED_EDGE ( 'NONE', *, *, #7998, .F. ) ;
#12721=CARTESIAN_POINT ( 'NONE',  ( 12.69999999999999929, -3604.958499999999731, 2290.241799999999785 ) ) ;
#12767=APPLICATION_CONTEXT ( 'configuration controlled 3d designs of mechanical parts and assemblies' ) ;
#12805=CIRCLE ( 'NONE', #18778, 5.460999999999938126 ) ;
#12809=CIRCLE ( 'NONE', #14690, 0.3809999999999647002 ) ;
#12858=VECTOR ( 'NONE', #431, 1000.000000000000000 ) ;
#12883=CARTESIAN_POINT ( 'NONE',  ( 12.69999999999999929, -3599.497499999999945, 2290.241799999999785 ) ) ;
#12920=AXIS2_PLACEMENT_3D ( 'NONE', #3808, #18223, #5700 ) ;
#12966=PLANE ( 'NONE',  #11947 ) ;
#12975=DIRECTION ( 'NONE',  ( 2.236068172604000108E-13, -1.295098308114000000E-13, 1.000000000000000000 ) ) ;
#13032=VERTEX_POINT ( 'NONE', #21151 ) ;
#13048=DIRECTION ( 'NONE',  ( 0.000000000000000000, -1.000000000000000000, 0.000000000000000000 ) ) ;
#13050=CARTESIAN_POINT ( 'NONE',  ( 12.69999999999999929, -3594.036500000000160, 2296.210799999999836 ) ) ;
#13148=EDGE_CURVE ( 'NONE', #22010, #3639, #3161, .T. ) ;
#13172=DIRECTION ( 'NONE',  ( -1.000000000000000000, 5.461016542361937364E-28, 2.336881798970999789E-14 ) ) ;
#13173=ORIENTED_EDGE ( 'NONE', *, *, #13148, .T. ) ;
#13240=EDGE_LOOP ( 'NONE', ( #22068, #1577, #20585, #6870 ) ) ;
#13302=DIRECTION ( 'NONE',  ( -2.301834883556000307E-13, -1.295098308109999907E-13, 1.000000000000000000 ) ) ;
#13377=VECTOR ( 'NONE', #5172, 1000.000000000000000 ) ;
#13393=CARTESIAN_POINT ( 'NONE',  ( 12.69999999999999929, -3599.497499999999945, 2263.571799999999712 ) ) ;
#13437=ORIENTED_EDGE ( 'NONE', *, *, #15232, .T. ) ;
#13486=DIRECTION ( 'NONE',  ( 0.000000000000000000, 0.000000000000000000, 1.000000000000000000 ) ) ;
#13491=VERTEX_POINT ( 'NONE', #13050 ) ;
#13505=AXIS2_PLACEMENT_3D ( 'NONE', #9551, #652, #7801 ) ;
#13534=EDGE_CURVE ( 'NONE', #7479, #13971, #6715, .T. ) ;
#13539=CARTESIAN_POINT ( 'NONE',  ( 12.69999999999999929, -3602.672500000000127, 2264.841800000000148 ) ) ;
#13540=CIRCLE ( 'NONE', #3436, 3.175000000000149925 ) ;
#13653=CARTESIAN_POINT ( 'NONE',  ( 15.41268679701173738, -3597.931329547518999, 2296.591799999999694 ) ) ;
#13695=DIRECTION ( 'NONE',  ( 1.000000000000000000, 0.000000000000000000, -2.336881798971000105E-14 ) ) ;
#13717=DIRECTION ( 'NONE',  ( 9.713237310828999775E-14, 5.180393232441999927E-13, 1.000000000000000000 ) ) ;
#13753=AXIS2_PLACEMENT_3D ( 'NONE', #16463, #417, #21966 ) ;
#13763=ORIENTED_EDGE ( 'NONE', *, *, #6579, .F. ) ;
#13798=MANIFOLD_SOLID_BREP ( 'SOLID22[1]', #22930 ) ;
#13806=CARTESIAN_POINT ( 'NONE',  ( 10.21049783562838265, -3600.934814744884534, 2296.591799999930117 ) ) ;
#13847=ORIENTED_EDGE ( 'NONE', *, *, #14140, .T. ) ;
#13962=ORIENTED_EDGE ( 'NONE', *, *, #20878, .T. ) ;
#13971=VERTEX_POINT ( 'NONE', #2414 ) ;
#13984=EDGE_CURVE ( 'NONE', #6446, #11488, #9087, .T. ) ;
#14021=EDGE_CURVE ( 'NONE', #23163, #2067, #6287, .T. ) ;
#14099=DIRECTION ( 'NONE',  ( 0.5000000000047110094, -0.8660254037817188832, 0.000000000000000000 ) ) ;
#14120=CARTESIAN_POINT ( 'NONE',  ( 12.69999999999999929, -3601.402499999999691, 2264.841800000000148 ) ) ;
#14140=EDGE_CURVE ( 'NONE', #17496, #7479, #17039, .T. ) ;
#14214=FACE_OUTER_BOUND ( 'NONE', #5269, .T. ) ;
#14228=EDGE_CURVE ( 'NONE', #6140, #3526, #5331, .T. ) ;
#14233=EDGE_CURVE ( 'NONE', #19050, #11590, #7588, .T. ) ;
#14236=CARTESIAN_POINT ( 'NONE',  ( 12.69999999999999929, -3602.672500000000127, 2264.841800000000148 ) ) ;
#14308=CARTESIAN_POINT ( 'NONE',  ( 12.69999999999999929, -3599.497499999999945, 2296.210799999999836 ) ) ;
#14311=EDGE_LOOP ( 'NONE', ( #1975, #9453, #9640, #14710 ) ) ;
#14313=EDGE_CURVE ( 'NONE', #10134, #5650, #7205, .T. ) ;
#14554=LINE ( 'NONE', #16070, #21026 ) ;
#14559=ADVANCED_FACE ( 'NONE', ( #2607 ), #18547, .T. ) ;
#14576=ORIENTED_EDGE ( 'NONE', *, *, #19514, .T. ) ;
#14596=EDGE_CURVE ( 'NONE', #15211, #8549, #11705, .T. ) ;
#14606=DIRECTION ( 'NONE',  ( 2.902585187577999742E-13, 4.457650181899999573E-12, -1.000000000000000000 ) ) ;
#14637=DIRECTION ( 'NONE',  ( -0.8660254037821902839, -0.5000000000038942183, 0.000000000000000000 ) ) ;
#14690=AXIS2_PLACEMENT_3D ( 'NONE', #16420, #7627, #9286 ) ;
#14710=ORIENTED_EDGE ( 'NONE', *, *, #3254, .F. ) ;
#14717=FACE_OUTER_BOUND ( 'NONE', #1457, .T. ) ;
#14719=AXIS2_PLACEMENT_3D ( 'NONE', #14308, #10899, #7390 ) ;
#14734=VERTEX_POINT ( 'NONE', #11261 ) ;
#14749=EDGE_CURVE ( 'NONE', #14916, #15211, #12809, .T. ) ;
#14809=CARTESIAN_POINT ( 'NONE',  ( 12.69999999999999929, -3599.497499999999945, 2296.210799999999836 ) ) ;
#14813=DIRECTION ( 'NONE',  ( 0.000000000000000000, 0.000000000000000000, -1.000000000000000000 ) ) ;
#14873=DIRECTION ( 'NONE',  ( 0.8660254037817188832, 0.5000000000047110094, -3.192239903041070306E-14 ) ) ;
#14916=VERTEX_POINT ( 'NONE', #1515 ) ;
#15055=CARTESIAN_POINT ( 'NONE',  ( 12.69999999996000106, -3602.189899999999852, 2292.781800000000203 ) ) ;
#15068=CARTESIAN_POINT ( 'NONE',  ( 12.69999999999999929, -3599.497499999999945, 2296.210799999999836 ) ) ;
#15083=EDGE_LOOP ( 'NONE', ( #2156, #5353, #18077, #7756 ) ) ;
#15125=CARTESIAN_POINT ( 'NONE',  ( 15.03168679714000078, -3598.151299999999992, 2292.781800000000203 ) ) ;
#15151=EDGE_LOOP ( 'NONE', ( #3854, #16736, #15226, #22827 ) ) ;
#15158=LINE ( 'NONE', #18777, #3282 ) ;
#15181=FACE_OUTER_BOUND ( 'NONE', #15151, .T. ) ;
#15211=VERTEX_POINT ( 'NONE', #4890 ) ;
#15226=ORIENTED_EDGE ( 'NONE', *, *, #21178, .T. ) ;
#15232=EDGE_CURVE ( 'NONE', #523, #3526, #5480, .T. ) ;
#15235=AXIS2_PLACEMENT_3D ( 'NONE', #4663, #1025, #20597 ) ;
#15240=FACE_OUTER_BOUND ( 'NONE', #5155, .T. ) ;
#15317=DIRECTION ( 'NONE',  ( 0.000000000000000000, -1.000000000000000000, 0.000000000000000000 ) ) ;
#15320=DIRECTION ( 'NONE',  ( -1.622664945668000106E-12, -1.000000000000000000, 0.000000000000000000 ) ) ;
#15334=DIRECTION ( 'NONE',  ( 2.336881798971000105E-14, 2.336881798971000105E-14, 1.000000000000000000 ) ) ;
#15387=LINE ( 'NONE', #19138, #2324 ) ;
#15429=CARTESIAN_POINT ( 'NONE',  ( 12.70000000023333264, -3602.629840905158289, 2296.591799999999694 ) ) ;
#15431=FACE_OUTER_BOUND ( 'NONE', #18817, .T. ) ;
#15450=VECTOR ( 'NONE', #6395, 999.9999999999998863 ) ;
#15470=CARTESIAN_POINT ( 'NONE',  ( 12.69999999996000106, -3602.189899999999852, 2292.781800000000203 ) ) ;
#15484=DIRECTION ( 'NONE',  ( 1.000000000000000000, -2.848812946084999742E-12, 0.000000000000000000 ) ) ;
#15500=DIRECTION ( 'NONE',  ( 0.000000000000000000, -1.000000000000000000, 0.000000000000000000 ) ) ;
#15505=DIRECTION ( 'NONE',  ( 0.8660254037820102058, 0.5000000000042060799, 0.000000000000000000 ) ) ;
#15526=CIRCLE ( 'NONE', #556, 5.080000000000000959 ) ;
#15585=ORIENTED_EDGE ( 'NONE', *, *, #7998, .T. ) ;
#15639=ORIENTED_EDGE ( 'NONE', *, *, #8090, .T. ) ;
#15683=CARTESIAN_POINT ( 'NONE',  ( 15.03168679714000078, -3598.151299999999992, 2292.781800000000203 ) ) ;
#15724=DIRECTION ( 'NONE',  ( -7.093784530908000077E-13, -1.000000000000000000, -3.793660610171000449E-12 ) ) ;
#15737=EDGE_CURVE ( 'NONE', #22010, #1650, #10135, .T. ) ;
#15742=CARTESIAN_POINT ( 'NONE',  ( 11.34365660141000021, -3601.846755679000125, 2296.210799999999836 ) ) ;
#15821=VECTOR ( 'NONE', #5104, 1000.000000000000227 ) ;
#15830=EDGE_CURVE ( 'NONE', #14734, #523, #19628, .T. ) ;
#15872=DIRECTION ( 'NONE',  ( 1.000000000000000000, 1.224646799147353207E-16, 0.000000000000000000 ) ) ;
#15923=VECTOR ( 'NONE', #22856, 1000.000000000000000 ) ;
#15934=CIRCLE ( 'NONE', #17038, 3.175000000000149925 ) ;
#15949=AXIS2_PLACEMENT_3D ( 'NONE', #22215, #18598, #4765 ) ;
#15956=CARTESIAN_POINT ( 'NONE',  ( 12.69999999999999929, -3599.497499999999945, 2290.622800000000097 ) ) ;
#16023=EDGE_CURVE ( 'NONE', #22010, #10134, #13540, .T. ) ;
#16032=ADVANCED_FACE ( 'NONE', ( #8362 ), #10105, .T. ) ;
#16070=CARTESIAN_POINT ( 'NONE',  ( 12.69999999994000106, -3596.365159094999854, 2296.591799999999694 ) ) ;
#16073=DIRECTION ( 'NONE',  ( 3.005032793049999585E-13, -2.590196616230999943E-13, -1.000000000000000000 ) ) ;
#16075=EDGE_CURVE ( 'NONE', #17394, #10503, #15387, .T. ) ;
#16077=DIRECTION ( 'NONE',  ( 0.5000000000007065459, 0.8660254037840305896, 0.000000000000000000 ) ) ;
#16085=PRODUCT_DEFINITION_FORMATION_WITH_SPECIFIED_SOURCE ( 'ANY', '', #6959, .NOT_KNOWN. ) ;
#16095=ORIENTED_EDGE ( 'NONE', *, *, #20166, .F. ) ;
#16199=CARTESIAN_POINT ( 'NONE',  ( 10.36831320284000135, -3598.151299999999992, 2292.781800000000203 ) ) ;
#16206=AXIS2_PLACEMENT_3D ( 'NONE', #20226, #83, #21754 ) ;
#16208=ORIENTED_EDGE ( 'NONE', *, *, #12393, .F. ) ;
#16272=AXIS2_PLACEMENT_3D ( 'NONE', #14120, #15872, #22654 ) ;
#16362=DIRECTION ( 'NONE',  ( 0.000000000000000000, -1.000000000000000000, 0.000000000000000000 ) ) ;
#16377=AXIS2_PLACEMENT_3D ( 'NONE', #17841, #8937, #21252 ) ;
#16378=DIRECTION ( 'NONE',  ( -1.224646799141892071E-16, -1.000000000000000000, 2.336881798971000421E-14 ) ) ;
#16420=CARTESIAN_POINT ( 'NONE',  ( 7.619999999999999218, -3599.497499999999945, 2290.622800000000097 ) ) ;
#16462=( GEOMETRIC_REPRESENTATION_CONTEXT ( 3 ) GLOBAL_UNCERTAINTY_ASSIGNED_CONTEXT ( ( #9258 ) ) GLOBAL_UNIT_ASSIGNED_CONTEXT ( ( #17942, #17480, #21592 ) ) REPRESENTATION_CONTEXT ( 'NONE', 'WORKASPACE' ) );
#16463=CARTESIAN_POINT ( 'NONE',  ( 12.69999999999999929, -3599.497499999999945, 2264.841800000000148 ) ) ;
#16490=DIRECTION ( 'NONE',  ( -1.000000000000000000, 5.461016542361937364E-28, 2.336881798970999789E-14 ) ) ;
#16521=EDGE_CURVE ( 'NONE', #19453, #22298, #21195, .T. ) ;
#16597=ADVANCED_FACE ( 'NONE', ( #9118 ), #16904, .T. ) ;
#16630=CARTESIAN_POINT ( 'NONE',  ( 10.36831320283682167, -3598.151299999850380, 2296.433984632765714 ) ) ;
#16636=CIRCLE ( 'NONE', #6554, 5.080000000000000071 ) ;
#16638=VECTOR ( 'NONE', #1943, 1000.000000000000000 ) ;
#16673=VECTOR ( 'NONE', #15320, 1000.000000000000000 ) ;
#16676=PRODUCT_CONTEXT ( 'NONE', #12767, 'mechanical' ) ;
#16736=ORIENTED_EDGE ( 'NONE', *, *, #9428, .F. ) ;
#16741=UNCERTAINTY_MEASURE_WITH_UNIT (LENGTH_MEASURE( 1.000000000000000082E-05 ), #21126, 'distance_accuracy_value', 'NONE');
#16771=CARTESIAN_POINT ( 'NONE',  ( 12.69999999999999929, -3594.036500000000160, 2290.241799999999785 ) ) ;
#16799=CARTESIAN_POINT ( 'NONE',  ( 10.36831320283000046, -3600.843699999999899, 2292.781800000000203 ) ) ;
#16844=EDGE_LOOP ( 'NONE', ( #11469, #13173, #21238, #8553 ) ) ;
#16904=TOROIDAL_SURFACE ( 'NONE', #811, 1.905000000000000027, 1.270000000000000018 ) ;
#16965=EDGE_CURVE ( 'NONE', #20602, #2972, #12805, .T. ) ;
#17021=AXIS2_PLACEMENT_3D ( 'NONE', #16799, #15484, #2944 ) ;
#17038=AXIS2_PLACEMENT_3D ( 'NONE', #18623, #2569, #798 ) ;
#17039=LINE ( 'NONE', #11536, #15450 ) ;
#17041=CARTESIAN_POINT ( 'NONE',  ( 15.03168679706394428, -3598.151299999898129, 2296.210799999999836 ) ) ;
#17065=DIRECTION ( 'NONE',  ( 0.000000000000000000, 0.000000000000000000, -1.000000000000000000 ) ) ;
#17094=EDGE_LOOP ( 'NONE', ( #11373, #13437, #4234, #677 ) ) ;
#17098=DIRECTION ( 'NONE',  ( 1.000000000000000000, 0.000000000000000000, -2.336881798971000105E-14 ) ) ;
#17143=ORIENTED_EDGE ( 'NONE', *, *, #8064, .T. ) ;
#17174=CARTESIAN_POINT ( 'NONE',  ( 12.69999999999133955, -3602.189900000167654, 2296.433984632682041 ) ) ;
#17177=DIRECTION ( 'NONE',  ( -2.336881798971000105E-14, 0.000000000000000000, -1.000000000000000000 ) ) ;
#17187=CARTESIAN_POINT ( 'NONE',  ( 9.987313202947220248, -3601.063670452640054, 2296.591799999999694 ) ) ;
#17228=CARTESIAN_POINT ( 'NONE',  ( 12.69999999999999929, -3599.497499999999945, 2264.841800000000148 ) ) ;
#17230=PLANE ( 'NONE',  #17021 ) ;
#17247=CARTESIAN_POINT ( 'NONE',  ( 12.69999999999999929, -3594.036500000000160, 2290.622800000000097 ) ) ;
#17341=FACE_OUTER_BOUND ( 'NONE', #19823, .T. ) ;
#17360=DIRECTION ( 'NONE',  ( 0.000000000000000000, 0.000000000000000000, 1.000000000000000000 ) ) ;
#17391=ORIENTED_EDGE ( 'NONE', *, *, #21630, .F. ) ;
#17394=VERTEX_POINT ( 'NONE', #11722 ) ;
#17429=( BOUNDED_CURVE ( )  B_SPLINE_CURVE ( 3, ( #11504, #7773, #2384, #22050 ),
 .UNSPECIFIED., .F., .F. ) 
 B_SPLINE_CURVE_WITH_KNOTS ( ( 4, 4 ),
 ( -9.769962616701377556E-15, 1.570796326960964162 ),
 .UNSPECIFIED. ) 
 CURVE ( )  GEOMETRIC_REPRESENTATION_ITEM ( )  RATIONAL_B_SPLINE_CURVE ( ( 1.000000000000000000, 0.8047378540852202500, 0.8047378540852202500, 1.000000000000000000 ) ) 
 REPRESENTATION_ITEM ( '' )  );
#17447=CARTESIAN_POINT ( 'NONE',  ( 12.69999999999981988, -3602.672500000000127, 2290.241799999999785 ) ) ;
#17459=LINE ( 'NONE', #22611, #13377 ) ;
#17468=ORIENTED_EDGE ( 'NONE', *, *, #14749, .F. ) ;
#17480=( NAMED_UNIT ( * ) PLANE_ANGLE_UNIT ( ) SI_UNIT ( $, .RADIAN. ) );
#17496=VERTEX_POINT ( 'NONE', #126 ) ;
#17539=ADVANCED_FACE ( 'NONE', ( #21574 ), #1233, .T. ) ;
#17622=CIRCLE ( 'NONE', #13505, 1.269999999999882334 ) ;
#17659=DIRECTION ( 'NONE',  ( 0.8660254037840939834, -0.5000000000005969669, 0.000000000000000000 ) ) ;
#17661=CARTESIAN_POINT ( 'NONE',  ( 12.69999999999999929, -3599.497499999999945, 2296.591799999999694 ) ) ;
#17670=AXIS2_PLACEMENT_3D ( 'NONE', #2899, #1129, #3125 ) ;
#17682=ORIENTED_EDGE ( 'NONE', *, *, #6579, .T. ) ;
#17748=CARTESIAN_POINT ( 'NONE',  ( 12.69999999996000106, -3602.629840905000037, 2296.591799999999694 ) ) ;
#17841=CARTESIAN_POINT ( 'NONE',  ( 15.41268679713999923, -3599.497499999999945, 2296.210799999999836 ) ) ;
#17873=AXIS2_PLACEMENT_3D ( 'NONE', #12883, #348, #19803 ) ;
#17942=( LENGTH_UNIT ( ) NAMED_UNIT ( * ) SI_UNIT ( .MILLI., .METRE. ) );
#17964=ORIENTED_EDGE ( 'NONE', *, *, #4790, .T. ) ;
#17980=ORIENTED_EDGE ( 'NONE', *, *, #3784, .F. ) ;
#17992=LINE ( 'NONE', #12721, #16638 ) ;
#17995=CARTESIAN_POINT ( 'NONE',  ( 10.36831320284000135, -3595.458900000000085, 2292.781800000000203 ) ) ;
#18037=ADVANCED_FACE ( 'NONE', ( #1340 ), #8504, .T. ) ;
#18056=SHAPE_REPRESENTATION ( 'Screw 3', ( #5611 ), #16462 ) ;
#18077=ORIENTED_EDGE ( 'NONE', *, *, #2430, .F. ) ;
#18101=CARTESIAN_POINT ( 'NONE',  ( 12.69999999999999929, -3599.497499999999945, 2296.210799999999836 ) ) ;
#18112=CARTESIAN_POINT ( 'NONE',  ( 9.987313202947220248, -3601.063670452640054, 2296.591799999999694 ) ) ;
#18132=DIRECTION ( 'NONE',  ( 2.336881798971000105E-14, 2.336881798971000105E-14, 1.000000000000000000 ) ) ;
#18140=LINE ( 'NONE', #5964, #2436 ) ;
#18223=DIRECTION ( 'NONE',  ( -0.5000000000040877302, 0.8660254037820785955, 0.000000000000000000 ) ) ;
#18325=SHAPE_DEFINITION_REPRESENTATION ( #3388, #18056 ) ;
#18400=CARTESIAN_POINT ( 'NONE',  ( 12.69999999999999929, -3599.497499999999945, 2263.571799999999712 ) ) ;
#18406=LINE ( 'NONE', #2362, #5520 ) ;
#18424=ORIENTED_EDGE ( 'NONE', *, *, #2007, .F. ) ;
#18517=TOROIDAL_SURFACE ( 'NONE', #6185, 5.080000000000000071, 0.3810000000000000053 ) ;
#18537=ADVANCED_FACE ( 'NONE', ( #22818 ), #3902, .T. ) ;
#18547=CYLINDRICAL_SURFACE ( 'NONE', #8735, 0.3809999999999993947 ) ;
#18564=FACE_OUTER_BOUND ( 'NONE', #1292, .T. ) ;
#18598=DIRECTION ( 'NONE',  ( 2.336881798971000105E-14, 2.336881798971000105E-14, 1.000000000000000000 ) ) ;
#18608=CIRCLE ( 'NONE', #13753, 3.175000000000149925 ) ;
#18623=CARTESIAN_POINT ( 'NONE',  ( 12.69999999999999929, -3599.497499999999945, 2290.241799999999785 ) ) ;
#18632=PLANE ( 'NONE',  #18769 ) ;
#18647=FACE_OUTER_BOUND ( 'NONE', #13240, .T. ) ;
#18676=ADVANCED_FACE ( 'NONE', ( #5503 ), #9519, .T. ) ;
#18696=CARTESIAN_POINT ( 'NONE',  ( 12.69999999997562057, -3602.189900000083526, 2296.210799999999836 ) ) ;
#18708=CARTESIAN_POINT ( 'NONE',  ( 10.36831320284000135, -3598.151299999999992, 2296.210799999999836 ) ) ;
#18763=ORIENTED_EDGE ( 'NONE', *, *, #14749, .T. ) ;
#18769=AXIS2_PLACEMENT_3D ( 'NONE', #18400, #20389, #2357 ) ;
#18777=CARTESIAN_POINT ( 'NONE',  ( 15.03168679714000078, -3598.151299999999992, 2292.781800000000203 ) ) ;
#18778=AXIS2_PLACEMENT_3D ( 'NONE', #18101, #302, #21393 ) ;
#18817=EDGE_LOOP ( 'NONE', ( #10701, #9749, #15639, #6000, #3384 ) ) ;
#18882=AXIS2_PLACEMENT_3D ( 'NONE', #21401, #3693, #19995 ) ;
#18961=AXIS2_PLACEMENT_3D ( 'NONE', #3400, #1875, #2117 ) ;
#19001=AXIS2_PLACEMENT_3D ( 'NONE', #11599, #2144, #11160 ) ;
#19033=ORIENTED_EDGE ( 'NONE', *, *, #19816, .T. ) ;
#19038=ADVANCED_FACE ( 'NONE', ( #14717 ), #2182, .T. ) ;
#19050=VERTEX_POINT ( 'NONE', #7450 ) ;
#19077=CARTESIAN_POINT ( 'NONE',  ( 12.69999999994000106, -3596.805100000000039, 2296.210799999999836 ) ) ;
#19100=LINE ( 'NONE', #15470, #21569 ) ;
#19115=EDGE_CURVE ( 'NONE', #4467, #14916, #9907, .T. ) ;
#19119=EDGE_CURVE ( 'NONE', #11590, #20602, #17992, .T. ) ;
#19138=CARTESIAN_POINT ( 'NONE',  ( 15.41268679713999923, -3601.063670452999759, 2296.591799999999694 ) ) ;
#19155=EDGE_LOOP ( 'NONE', ( #6573, #17964, #11481, #10823, #17468 ) ) ;
#19253=ADVANCED_FACE ( 'NONE', ( #17341 ), #18517, .T. ) ;
#19255=CARTESIAN_POINT ( 'NONE',  ( 12.69999999999999929, -3599.497499999999945, 2264.841800000000148 ) ) ;
#19271=EDGE_CURVE ( 'NONE', #17496, #19453, #4934, .T. ) ;
#19275=CARTESIAN_POINT ( 'NONE',  ( 15.41268679701173738, -3597.931329547518999, 2296.591799999999694 ) ) ;
#19285=DIRECTION ( 'NONE',  ( 0.000000000000000000, 0.000000000000000000, 1.000000000000000000 ) ) ;
#19309=ADVANCED_FACE ( 'NONE', ( #18564 ), #17230, .T. ) ;
#19360=( BOUNDED_CURVE ( )  B_SPLINE_CURVE ( 3, ( #17041, #1104, #22424, #13653 ),
 .UNSPECIFIED., .F., .F. ) 
 B_SPLINE_CURVE_WITH_KNOTS ( ( 4, 4 ),
 ( -2.664535259100375697E-14, 1.570796326280532895 ),
 .UNSPECIFIED. ) 
 CURVE ( )  GEOMETRIC_REPRESENTATION_ITEM ( )  RATIONAL_B_SPLINE_CURVE ( ( 1.000000000000000000, 0.8047378542455954076, 0.8047378542455954076, 1.000000000000000000 ) ) 
 REPRESENTATION_ITEM ( '' )  );
#19396=CARTESIAN_POINT ( 'NONE',  ( 17.78000000000000114, -3599.497499999999945, 2296.210799999999836 ) ) ;
#19419=CARTESIAN_POINT ( 'NONE',  ( 12.69999999996000106, -3602.189899999999852, 2292.781800000000203 ) ) ;
#19453=VERTEX_POINT ( 'NONE', #5880 ) ;
#19458=CYLINDRICAL_SURFACE ( 'NONE', #18961, 0.3809999999998115450 ) ;
#19506=DIRECTION ( 'NONE',  ( 0.000000000000000000, -1.000000000000000000, 0.000000000000000000 ) ) ;
#19514=EDGE_CURVE ( 'NONE', #14916, #4467, #15526, .T. ) ;
#19546=EDGE_CURVE ( 'NONE', #1150, #13971, #21487, .T. ) ;
#19602=FACE_OUTER_BOUND ( 'NONE', #7831, .T. ) ;
#19614=DIRECTION ( 'NONE',  ( 0.000000000000000000, 2.336881798971000105E-14, 1.000000000000000000 ) ) ;
#19628=LINE ( 'NONE', #17748, #2675 ) ;
#19680=CIRCLE ( 'NONE', #22653, 5.460999999999938126 ) ;
#19686=AXIS2_PLACEMENT_3D ( 'NONE', #17661, #15334, #13695 ) ;
#19803=DIRECTION ( 'NONE',  ( 0.000000000000000000, -1.000000000000000000, 0.000000000000000000 ) ) ;
#19816=EDGE_CURVE ( 'NONE', #2067, #6140, #11580, .T. ) ;
#19823=EDGE_LOOP ( 'NONE', ( #4019, #10213, #18763, #21563, #2327 ) ) ;
#19874=CARTESIAN_POINT ( 'NONE',  ( 10.36831320289432057, -3600.843700000111312, 2296.210799999999836 ) ) ;
#19886=CARTESIAN_POINT ( 'NONE',  ( 12.69999999994000106, -3596.805100000000039, 2292.781800000000203 ) ) ;
#19995=DIRECTION ( 'NONE',  ( 1.000000000000000000, 0.000000000000000000, 0.000000000000000000 ) ) ;
#20016=DIRECTION ( 'NONE',  ( 0.000000000000000000, 1.000000000000000000, 0.000000000000000000 ) ) ;
#20141=ADVANCED_FACE ( 'NONE', ( #15431 ), #9945, .T. ) ;
#20161=EDGE_LOOP ( 'NONE', ( #4448, #2544 ) ) ;
#20166=EDGE_CURVE ( 'NONE', #8549, #19050, #7696, .T. ) ;
#20170=PLANE ( 'NONE',  #21418 ) ;
#20191=EDGE_LOOP ( 'NONE', ( #17980, #21521, #9912, #20832, #17391, #22965 ) ) ;
#20226=CARTESIAN_POINT ( 'NONE',  ( 7.619999999999999218, -3599.497499999999945, 2296.210799999999836 ) ) ;
#20251=DIRECTION ( 'NONE',  ( 0.000000000000000000, -1.000000000000000000, 0.000000000000000000 ) ) ;
#20295=LINE ( 'NONE', #16771, #3270 ) ;
#20309=AXIS2_PLACEMENT_3D ( 'NONE', #19886, #5487, #5601 ) ;
#20352=ORIENTED_EDGE ( 'NONE', *, *, #13148, .F. ) ;
#20389=DIRECTION ( 'NONE',  ( 0.000000000000000000, 0.000000000000000000, 1.000000000000000000 ) ) ;
#20543=CARTESIAN_POINT ( 'NONE',  ( 12.69999999999999929, -3599.497499999999945, 2296.591799999999694 ) ) ;
#20585=ORIENTED_EDGE ( 'NONE', *, *, #2150, .F. ) ;
#20597=DIRECTION ( 'NONE',  ( 0.000000000000000000, -1.000000000000000000, 0.000000000000000000 ) ) ;
#20602=VERTEX_POINT ( 'NONE', #20909 ) ;
#20824=EDGE_CURVE ( 'NONE', #11488, #9357, #16636, .T. ) ;
#20832=ORIENTED_EDGE ( 'NONE', *, *, #19119, .T. ) ;
#20878=EDGE_CURVE ( 'NONE', #2067, #17394, #17429, .T. ) ;
#20909=CARTESIAN_POINT ( 'NONE',  ( 12.69999999999999929, -3604.958499999999731, 2296.210799999999836 ) ) ;
#20955=CARTESIAN_POINT ( 'NONE',  ( 17.77999999999999758, -3599.497499999999945, 2290.241799999999785 ) ) ;
#21003=ORIENTED_EDGE ( 'NONE', *, *, #20878, .F. ) ;
#21026=VECTOR ( 'NONE', #5298, 1000.000000000000000 ) ;
#21079=AXIS2_PLACEMENT_3D ( 'NONE', #15068, #7687, #2415 ) ;
#21081=ORIENTED_EDGE ( 'NONE', *, *, #2150, .T. ) ;
#21102=CARTESIAN_POINT ( 'NONE',  ( 12.69999999971559212, -3596.365159094870251, 2296.591799999999694 ) ) ;
#21126=( LENGTH_UNIT ( ) NAMED_UNIT ( * ) SI_UNIT ( .MILLI., .METRE. ) );
#21132=DIRECTION ( 'NONE',  ( 0.000000000000000000, 0.000000000000000000, -1.000000000000000000 ) ) ;
#21151=CARTESIAN_POINT ( 'NONE',  ( 12.69999999996000106, -3602.189899999999852, 2292.781800000000203 ) ) ;
#21178=EDGE_CURVE ( 'NONE', #2888, #23163, #6712, .T. ) ;
#21195=LINE ( 'NONE', #19077, #4210 ) ;
#21238=ORIENTED_EDGE ( 'NONE', *, *, #10833, .F. ) ;
#21246=EDGE_CURVE ( 'NONE', #11590, #15211, #7679, .T. ) ;
#21252=DIRECTION ( 'NONE',  ( 1.000000000000000000, -1.165588477296748772E-12, 0.000000000000000000 ) ) ;
#21274=CARTESIAN_POINT ( 'NONE',  ( 12.69999999999999929, -3599.497499999999945, 2290.622800000000097 ) ) ;
#21321=DIRECTION ( 'NONE',  ( -0.8660254037819670181, -0.5000000000042810200, 0.000000000000000000 ) ) ;
#21345=ORIENTED_EDGE ( 'NONE', *, *, #577, .T. ) ;
#21349=EDGE_CURVE ( 'NONE', #1150, #523, #11668, .T. ) ;
#21362=PLANE ( 'NONE',  #23100 ) ;
#21375=ORIENTED_EDGE ( 'NONE', *, *, #19816, .F. ) ;
#21393=DIRECTION ( 'NONE',  ( 0.000000000000000000, -1.000000000000000000, 0.000000000000000000 ) ) ;
#21401=CARTESIAN_POINT ( 'NONE',  ( 12.69999999999999929, -3599.497499999999945, 2290.241799999999785 ) ) ;
#21418=AXIS2_PLACEMENT_3D ( 'NONE', #2474, #4562, #17098 ) ;
#21434=CARTESIAN_POINT ( 'NONE',  ( 15.03168679714000078, -3600.843699999999899, 2296.210799999999836 ) ) ;
#21451=FACE_OUTER_BOUND ( 'NONE', #8724, .T. ) ;
#21487=( BOUNDED_CURVE ( )  B_SPLINE_CURVE ( 3, ( #9492, #7851, #16630, #588 ),
 .UNSPECIFIED., .F., .F. ) 
 B_SPLINE_CURVE_WITH_KNOTS ( ( 4, 4 ),
 ( 1.570796326625032657, 3.141592653589783346 ),
 .UNSPECIFIED. ) 
 CURVE ( )  GEOMETRIC_REPRESENTATION_ITEM ( )  RATIONAL_B_SPLINE_CURVE ( ( 1.000000000000000000, 0.8047378540843299621, 0.8047378540843299621, 1.000000000000000000 ) ) 
 REPRESENTATION_ITEM ( '' )  );
#21521=ORIENTED_EDGE ( 'NONE', *, *, #14596, .F. ) ;
#21554=ORIENTED_EDGE ( 'NONE', *, *, #15830, .T. ) ;
#21563=ORIENTED_EDGE ( 'NONE', *, *, #14596, .T. ) ;
#21569=VECTOR ( 'NONE', #13717, 1000.000000000000000 ) ;
#21574=FACE_OUTER_BOUND ( 'NONE', #9807, .T. ) ;
#21592=( NAMED_UNIT ( * ) SI_UNIT ( $, .STERADIAN. ) SOLID_ANGLE_UNIT ( ) );
#21630=EDGE_CURVE ( 'NONE', #6446, #20602, #19680, .T. ) ;
#21655=DIRECTION ( 'NONE',  ( 0.000000000000000000, 0.000000000000000000, -1.000000000000000000 ) ) ;
#21659=ORIENTED_EDGE ( 'NONE', *, *, #7864, .T. ) ;
#21727=EDGE_LOOP ( 'NONE', ( #10036, #23056, #387, #562 ) ) ;
#21754=DIRECTION ( 'NONE',  ( 0.000000000000000000, 0.000000000000000000, 1.000000000000000000 ) ) ;
#21757=( BOUNDED_CURVE ( )  B_SPLINE_CURVE ( 3, ( #8168, #17174, #7936, #15429 ),
 .UNSPECIFIED., .F., .T. ) 
 B_SPLINE_CURVE_WITH_KNOTS ( ( 4, 4 ),
 ( 3.686081134657729747E-14, 1.570796326492095440 ),
 .UNSPECIFIED. ) 
 CURVE ( )  GEOMETRIC_REPRESENTATION_ITEM ( )  RATIONAL_B_SPLINE_CURVE ( ( 1.000000000000000000, 0.8047378541957446174, 0.8047378541957446174, 1.000000000000000000 ) ) 
 REPRESENTATION_ITEM ( '' )  );
#21796=VECTOR ( 'NONE', #2218, 1000.000000000000114 ) ;
#21819=AXIS2_PLACEMENT_3D ( 'NONE', #19396, #12123, #3449 ) ;
#21908=CARTESIAN_POINT ( 'NONE',  ( 12.69999999999999929, -3596.322499999999764, 2290.241799999999785 ) ) ;
#21966=DIRECTION ( 'NONE',  ( 0.000000000000000000, 1.000000000000000000, 0.000000000000000000 ) ) ;
#22010=VERTEX_POINT ( 'NONE', #14236 ) ;
#22050=CARTESIAN_POINT ( 'NONE',  ( 15.41268679713999923, -3601.063670452857423, 2296.591799999999694 ) ) ;
#22068=ORIENTED_EDGE ( 'NONE', *, *, #3609, .F. ) ;
#22169=ORIENTED_EDGE ( 'NONE', *, *, #4065, .F. ) ;
#22215=CARTESIAN_POINT ( 'NONE',  ( 12.69999999999999929, -3599.497499999999945, 2296.210799999999836 ) ) ;
#22234=CIRCLE ( 'NONE', #6924, 5.080000000000000071 ) ;
#22279=CARTESIAN_POINT ( 'NONE',  ( 12.69999999999999929, -3599.497499999999945, 2290.622800000000097 ) ) ;
#22298=VERTEX_POINT ( 'NONE', #782 ) ;
#22383=ORIENTED_EDGE ( 'NONE', *, *, #14313, .F. ) ;
#22401=CARTESIAN_POINT ( 'NONE',  ( 12.69999999999999929, -3599.497499999999945, 2264.841800000000148 ) ) ;
#22424=CARTESIAN_POINT ( 'NONE',  ( 15.18950216430096667, -3598.060185255141732, 2296.591799999885097 ) ) ;
#22436=DIRECTION ( 'NONE',  ( 0.000000000000000000, 0.000000000000000000, -1.000000000000000000 ) ) ;
#22512=ADVANCED_FACE ( 'NONE', ( #4648 ), #12273, .T. ) ;
#22513=DIRECTION ( 'NONE',  ( -2.336881798971000105E-14, 0.000000000000000000, -1.000000000000000000 ) ) ;
#22569=CARTESIAN_POINT ( 'NONE',  ( 9.987313202835000681, -3597.931329546999677, 2296.591799999999694 ) ) ;
#22611=CARTESIAN_POINT ( 'NONE',  ( 10.36831320283000046, -3600.843699999999899, 2296.210799999999836 ) ) ;
#22643=ORIENTED_EDGE ( 'NONE', *, *, #2760, .T. ) ;
#22651=EDGE_LOOP ( 'NONE', ( #16095, #9615, #22903, #3013, #7966, #11998 ) ) ;
#22653=AXIS2_PLACEMENT_3D ( 'NONE', #11092, #7682, #16362 ) ;
#22654=DIRECTION ( 'NONE',  ( 0.000000000000000000, 1.000000000000000000, 0.000000000000000000 ) ) ;
#22758=ADVANCED_FACE ( 'NONE', ( #15181 ), #12966, .T. ) ;
#22818=FACE_OUTER_BOUND ( 'NONE', #19155, .T. ) ;
#22827=ORIENTED_EDGE ( 'NONE', *, *, #14021, .T. ) ;
#22856=DIRECTION ( 'NONE',  ( 3.424927947643999841E-13, 2.590196616239000129E-13, 1.000000000000000000 ) ) ;
#22903=ORIENTED_EDGE ( 'NONE', *, *, #918, .F. ) ;
#22930=CLOSED_SHELL ( 'NONE', ( #18676, #6840, #18537, #9001, #20141, #14559, #11547, #19309, #22512, #19038, #22758, #2252, #3660, #1858, #18037, #3702, #5529, #9649, #10267, #17539, #5716, #19253, #1547, #16032, #16597, #1524 ) ) ;
#22965=ORIENTED_EDGE ( 'NONE', *, *, #2383, .F. ) ;
#22974=CARTESIAN_POINT ( 'NONE',  ( 10.36831320284000135, -3598.151299999999992, 2292.781800000000203 ) ) ;
#23010=CARTESIAN_POINT ( 'NONE',  ( 12.69999999971559212, -3596.365159094870251, 2296.591799999999694 ) ) ;
#23056=ORIENTED_EDGE ( 'NONE', *, *, #19271, .F. ) ;
#23094=( NAMED_UNIT ( * ) SI_UNIT ( $, .STERADIAN. ) SOLID_ANGLE_UNIT ( ) );
#23100=AXIS2_PLACEMENT_3D ( 'NONE', #16199, #14099, #3766 ) ;
#23149=CARTESIAN_POINT ( 'NONE',  ( 10.36831320283000046, -3600.843699999999899, 2292.781800000000203 ) ) ;
#23163=VERTEX_POINT ( 'NONE', #2391 ) ;
#23208=COLOUR_RGB('Black',0.12,0.14,0.17);
#23209=FILL_AREA_STYLE_COLOUR('',#23208);
#23210=FILL_AREA_STYLE('',(#23209));
#23211=SURFACE_STYLE_FILL_AREA(#23210);
#23212=SURFACE_SIDE_STYLE('',(#23211));
#23213=SURFACE_STYLE_USAGE(.BOTH.,#23212);
#23214=PRESENTATION_STYLE_ASSIGNMENT((#23213));
#23223=STYLED_ITEM('',(#23214),#13798);
#23237=MECHANICAL_DESIGN_GEOMETRIC_PRESENTATION_REPRESENTATION('',(#23223),#2257);
ENDSEC;
END-ISO-10303-21;
